ISO-10303-21;
HEADER;
FILE_DESCRIPTION (('STEP AP214'),
    '1' );
FILE_NAME ('1.8 Handle Rod.step',
    '2026-10-06T08:51:13',
    ( '' ),
    ( '' ),
    'SwSTEP 2.0',
    'SolidWorks 2021',
    '' );
FILE_SCHEMA (( 'AUTOMOTIVE_DESIGN' ));
ENDSEC;

DATA;
#161=( NAMED_UNIT ( * ) PLANE_ANGLE_UNIT ( ) SI_UNIT ( $, .RADIAN. ) );
#331=( LENGTH_UNIT ( ) NAMED_UNIT ( * ) SI_UNIT ( .MILLI., .METRE. ) );
#1046=CARTESIAN_POINT ( 'NONE',  ( 0.000000000000000000, 60.00000000000000000, 0.000000000000000000 ) ) ;
#1179=EDGE_CURVE ( 'NONE', #76434, #9731, #45604, .T. ) ;
#1357=DIRECTION ( 'NONE',  ( 0.000000000000000000, 0.000000000000000000, 1.000000000000000000 ) ) ;
#1816=ORIENTED_EDGE ( 'NONE', *, *, #24259, .T. ) ;
#2531=AXIS2_PLACEMENT_3D ( 'NONE', #1046, #89511, #78644 ) ;
#3731=ADVANCED_FACE ( 'NONE', ( #28568 ), #116978, .F. ) ;
#4207=UNCERTAINTY_MEASURE_WITH_UNIT (LENGTH_MEASURE( 1.000000000000000082E-05 ), #53487, 'distance_accuracy_value', 'NONE');
#5231=CARTESIAN_POINT ( 'NONE',  ( 0.000000000000000000, -60.00000000000000000, 0.000000000000000000 ) ) ;
#5751=MECHANICAL_DESIGN_GEOMETRIC_PRESENTATION_REPRESENTATION('',(#89104),#121561);
#6113=MECHANICAL_DESIGN_GEOMETRIC_PRESENTATION_REPRESENTATION('',(#89567),#91836);
#6746=SURFACE_STYLE_FILL_AREA ( #106073 ) ;
#7174=( GEOMETRIC_REPRESENTATION_CONTEXT ( 3 ) GLOBAL_UNCERTAINTY_ASSIGNED_CONTEXT ( ( #56403 ) ) GLOBAL_UNIT_ASSIGNED_CONTEXT ( ( #331, #33734, #67058 ) ) REPRESENTATION_CONTEXT ( 'NONE', 'WORKASPACE' ) );
#7835=AXIS2_PLACEMENT_3D ( 'NONE', #110119, #33341, #123180 ) ;
#8144=EDGE_LOOP ( 'NONE', ( #45874, #39153 ) ) ;
#8925=CARTESIAN_POINT ( 'NONE',  ( 0.000000000000000000, 0.000000000000000000, 0.000000000000000000 ) ) ;
#9731=VERTEX_POINT ( 'NONE', #137997 ) ;
#13354=PRESENTATION_STYLE_ASSIGNMENT (( #143177 ) ) ;
#14391=( LENGTH_UNIT ( ) NAMED_UNIT ( * ) SI_UNIT ( .MILLI., .METRE. ) );
#15293=( NAMED_UNIT ( * ) PLANE_ANGLE_UNIT ( ) SI_UNIT ( $, .RADIAN. ) );
#16005=PRESENTATION_STYLE_ASSIGNMENT (( #116779 ) ) ;
#17956=SURFACE_SIDE_STYLE ('',( #130344 ) ) ;
#18145=SURFACE_STYLE_FILL_AREA ( #26917 ) ;
#18245=COLOUR_RGB ( '', 0.40784314, 0.44705882, 0.49803922) ;
#18771=EDGE_LOOP ( 'NONE', ( #74023, #38665, #1816, #108309 ) ) ;
#20500=DIRECTION ( 'NONE',  ( 0.000000000000000000, -0.000000000000000000, 1.000000000000000000 ) ) ;
#22631=PRESENTATION_STYLE_ASSIGNMENT (( #95225 ) ) ;
#22636=PRODUCT_DEFINITION ( 'UNKNOWN', '', #37846, #63247 ) ;
#24259=EDGE_CURVE ( 'NONE', #63418, #9731, #93314, .T. ) ;
#25470=AXIS2_PLACEMENT_3D ( 'NONE', #135364, #58550, #102718 ) ;
#25734=MECHANICAL_DESIGN_GEOMETRIC_PRESENTATION_REPRESENTATION('',(#58180),#7174);
#26239=COLOUR_RGB ( '', 0.40784314, 0.44705882, 0.49803922) ;
#26696=DIRECTION ( 'NONE',  ( -0.000000000000000000, -1.000000000000000000, -0.000000000000000000 ) ) ;
#26917=FILL_AREA_STYLE ('',( #115309 ) ) ;
#28080=SHAPE_REPRESENTATION_RELATIONSHIP ( 'NONE' , 'NONE' ,  #39429, #96673 ) ;
#28568=FACE_OUTER_BOUND ( 'NONE', #8144, .T. ) ;
#28670=EDGE_LOOP ( 'NONE', ( #79254, #115144, #48341, #68111 ) ) ;
#28844=DIRECTION ( 'NONE',  ( 0.000000000000000000, 0.000000000000000000, -1.000000000000000000 ) ) ;
#29756=ADVANCED_FACE ( 'NONE', ( #117978 ), #52748, .T. ) ;
#31111=EDGE_LOOP ( 'NONE', ( #82253, #89209 ) ) ;
#31875=CARTESIAN_POINT ( 'NONE',  ( 0.000000000000000000, 60.00000000000000000, 0.000000000000000000 ) ) ;
#32389=DIRECTION ( 'NONE',  ( -0.000000000000000000, -1.000000000000000000, -0.000000000000000000 ) ) ;
#32558=AXIS2_PLACEMENT_3D ( 'NONE', #31875, #101405, #1357 ) ;
#33341=DIRECTION ( 'NONE',  ( 0.000000000000000000, 1.000000000000000000, 0.000000000000000000 ) ) ;
#33734=( NAMED_UNIT ( * ) PLANE_ANGLE_UNIT ( ) SI_UNIT ( $, .RADIAN. ) );
#34012=PRODUCT_DEFINITION_SHAPE ( 'NONE', 'NONE',  #22636 ) ;
#36286=COLOUR_RGB ( '', 0.31764706, 0.68627451, 0.89019608) ;
#37171=DIRECTION ( 'NONE',  ( 0.000000000000000000, 1.000000000000000000, 0.000000000000000000 ) ) ;
#37373=AXIS2_PLACEMENT_3D ( 'NONE', #96940, #75260, #50628 ) ;
#37846=PRODUCT_DEFINITION_FORMATION_WITH_SPECIFIED_SOURCE ( 'ANY', '', #44431, .NOT_KNOWN. ) ;
#38665=ORIENTED_EDGE ( 'NONE', *, *, #43998, .F. ) ;
#39153=ORIENTED_EDGE ( 'NONE', *, *, #1179, .F. ) ;
#39429=SHAPE_REPRESENTATION ( '1.8 Handle Rod', ( #127880 ), #114185 ) ;
#40278=CIRCLE ( 'NONE', #7835, 4.000000000000000000 ) ;
#41092=SURFACE_STYLE_USAGE ( .BOTH. , #139728 ) ;
#41555=( NAMED_UNIT ( * ) SI_UNIT ( $, .STERADIAN. ) SOLID_ANGLE_UNIT ( ) );
#43998=EDGE_CURVE ( 'NONE', #63418, #115520, #40278, .T. ) ;
#44431=PRODUCT ( '1.8 Handle Rod', '1.8 Handle Rod', '', ( #83010 ) ) ;
#45604=CIRCLE ( 'NONE', #73330, 4.000000000000000000 ) ;
#45874=ORIENTED_EDGE ( 'NONE', *, *, #75552, .F. ) ;
#46024=UNCERTAINTY_MEASURE_WITH_UNIT (LENGTH_MEASURE( 1.000000000000000082E-05 ), #138273, 'distance_accuracy_value', 'NONE');
#46782=PLANE ( 'NONE',  #2531 ) ;
#48341=ORIENTED_EDGE ( 'NONE', *, *, #1179, .T. ) ;
#48446=SURFACE_STYLE_USAGE ( .BOTH. , #60797 ) ;
#49611=ADVANCED_FACE ( 'NONE', ( #112686 ), #46782, .T. ) ;
#50628=DIRECTION ( 'NONE',  ( 0.000000000000000000, 0.000000000000000000, -1.000000000000000000 ) ) ;
#50772=VECTOR ( 'NONE', #32389, 1000.000000000000000 ) ;
#51027=SURFACE_SIDE_STYLE ('',( #6746 ) ) ;
#51255=CARTESIAN_POINT ( 'NONE',  ( 0.000000000000000000, 60.00000000000000000, -4.000000000000000000 ) ) ;
#51274=( NAMED_UNIT ( * ) PLANE_ANGLE_UNIT ( ) SI_UNIT ( $, .RADIAN. ) );
#52060=FILL_AREA_STYLE_COLOUR ( '', #136913 ) ;
#52748=CYLINDRICAL_SURFACE ( 'NONE', #37373, 4.000000000000000000 ) ;
#53195=DIRECTION ( 'NONE',  ( 1.000000000000000000, 0.000000000000000000, 0.000000000000000000 ) ) ;
#53487=( LENGTH_UNIT ( ) NAMED_UNIT ( * ) SI_UNIT ( .MILLI., .METRE. ) );
#53519=MECHANICAL_DESIGN_GEOMETRIC_PRESENTATION_REPRESENTATION('',(#97470),#102165);
#56294=MECHANICAL_DESIGN_GEOMETRIC_PRESENTATION_REPRESENTATION('',(#111821),#128082);
#56403=UNCERTAINTY_MEASURE_WITH_UNIT (LENGTH_MEASURE( 1.000000000000000082E-05 ), #331, 'distance_accuracy_value', 'NONE');
#58180=STYLED_ITEM ( 'NONE', ( #13354 ), #49611 ) ;
#58203=CARTESIAN_POINT ( 'NONE',  ( 4.898587196589412829E-16, -60.00000000000000000, 4.000000000000000000 ) ) ;
#58550=DIRECTION ( 'NONE',  ( 0.000000000000000000, 1.000000000000000000, 0.000000000000000000 ) ) ;
#60797=SURFACE_SIDE_STYLE ('',( #91268 ) ) ;
#61921=FILL_AREA_STYLE_COLOUR ( '', #36286 ) ;
#63247=PRODUCT_DEFINITION_CONTEXT ( 'detailed design', #92057, 'design' ) ;
#63418=VERTEX_POINT ( 'NONE', #99433 ) ;
#65216=APPLICATION_CONTEXT ( 'automotive_design' ) ;
#67058=( NAMED_UNIT ( * ) SI_UNIT ( $, .STERADIAN. ) SOLID_ANGLE_UNIT ( ) );
#67822=UNCERTAINTY_MEASURE_WITH_UNIT (LENGTH_MEASURE( 1.000000000000000082E-05 ), #14391, 'distance_accuracy_value', 'NONE');
#68111=ORIENTED_EDGE ( 'NONE', *, *, #24259, .F. ) ;
#68331=AXIS2_PLACEMENT_3D ( 'NONE', #81830, #26696, #28844 ) ;
#69510=FACE_OUTER_BOUND ( 'NONE', #28670, .T. ) ;
#70252=( NAMED_UNIT ( * ) SI_UNIT ( $, .STERADIAN. ) SOLID_ANGLE_UNIT ( ) );
#70983=EDGE_CURVE ( 'NONE', #115520, #63418, #141297, .T. ) ;
#71595=( NAMED_UNIT ( * ) PLANE_ANGLE_UNIT ( ) SI_UNIT ( $, .RADIAN. ) );
#71883=CLOSED_SHELL ( 'NONE', ( #107309, #29756, #49611, #3731 ) ) ;
#73030=DIRECTION ( 'NONE',  ( -0.000000000000000000, -1.000000000000000000, -0.000000000000000000 ) ) ;
#73330=AXIS2_PLACEMENT_3D ( 'NONE', #5231, #37171, #82839 ) ;
#73720=( LENGTH_UNIT ( ) NAMED_UNIT ( * ) SI_UNIT ( .MILLI., .METRE. ) );
#74023=ORIENTED_EDGE ( 'NONE', *, *, #114060, .F. ) ;
#74825=UNCERTAINTY_MEASURE_WITH_UNIT (LENGTH_MEASURE( 1.000000000000000082E-05 ), #73720, 'distance_accuracy_value', 'NONE');
#75260=DIRECTION ( 'NONE',  ( -0.000000000000000000, -1.000000000000000000, -0.000000000000000000 ) ) ;
#75552=EDGE_CURVE ( 'NONE', #9731, #76434, #134373, .T. ) ;
#76434=VERTEX_POINT ( 'NONE', #58203 ) ;
#77999=AXIS2_PLACEMENT_3D ( 'NONE', #119810, #87924, #20500 ) ;
#78644=DIRECTION ( 'NONE',  ( 0.000000000000000000, -0.000000000000000000, 1.000000000000000000 ) ) ;
#79254=ORIENTED_EDGE ( 'NONE', *, *, #70983, .F. ) ;
#79406=SURFACE_SIDE_STYLE ('',( #99658 ) ) ;
#81830=CARTESIAN_POINT ( 'NONE',  ( 0.000000000000000000, 60.00000000000000000, 0.000000000000000000 ) ) ;
#82253=ORIENTED_EDGE ( 'NONE', *, *, #43998, .T. ) ;
#82839=DIRECTION ( 'NONE',  ( 0.000000000000000000, 0.000000000000000000, 1.000000000000000000 ) ) ;
#83010=PRODUCT_CONTEXT ( 'NONE', #65216, 'mechanical' ) ;
#83179=( NAMED_UNIT ( * ) SI_UNIT ( $, .STERADIAN. ) SOLID_ANGLE_UNIT ( ) );
#83456=SURFACE_SIDE_STYLE ('',( #18145 ) ) ;
#87924=DIRECTION ( 'NONE',  ( 0.000000000000000000, 1.000000000000000000, 0.000000000000000000 ) ) ;
#88252=COLOUR_RGB ( '', 0.66274510, 0.83137255, 0.94901961) ;
#89104=STYLED_ITEM ( 'NONE', ( #124580 ), #107309 ) ;
#89209=ORIENTED_EDGE ( 'NONE', *, *, #70983, .T. ) ;
#89511=DIRECTION ( 'NONE',  ( 0.000000000000000000, 1.000000000000000000, 0.000000000000000000 ) ) ;
#89567=STYLED_ITEM ( 'NONE', ( #22631 ), #3731 ) ;
#90964=FILL_AREA_STYLE_COLOUR ( '', #88252 ) ;
#91268=SURFACE_STYLE_FILL_AREA ( #104221 ) ;
#91836=( GEOMETRIC_REPRESENTATION_CONTEXT ( 3 ) GLOBAL_UNCERTAINTY_ASSIGNED_CONTEXT ( ( #129076 ) ) GLOBAL_UNIT_ASSIGNED_CONTEXT ( ( #99489, #161, #41555 ) ) REPRESENTATION_CONTEXT ( 'NONE', 'WORKASPACE' ) );
#92057=APPLICATION_CONTEXT ( 'automotive_design' ) ;
#93314=LINE ( 'NONE', #51255, #127824 ) ;
#93335=FILL_AREA_STYLE_COLOUR ( '', #26239 ) ;
#94809=FILL_AREA_STYLE ('',( #52060 ) ) ;
#95225=SURFACE_STYLE_USAGE ( .BOTH. , #51027 ) ;
#96673=ADVANCED_BREP_SHAPE_REPRESENTATION ( '', ( #139143, #127880 ), #114185 ) ;
#96940=CARTESIAN_POINT ( 'NONE',  ( 0.000000000000000000, 60.00000000000000000, 0.000000000000000000 ) ) ;
#97470=STYLED_ITEM ( 'NONE', ( #118726 ), #29756 ) ;
#98405=COLOUR_RGB ( '', 0.09019608, 0.27058824, 0.51372549) ;
#99284=STYLED_ITEM ( 'NONE', ( #16005 ), #139143 ) ;
#99433=CARTESIAN_POINT ( 'NONE',  ( 0.000000000000000000, 60.00000000000000000, -4.000000000000000000 ) ) ;
#99489=( LENGTH_UNIT ( ) NAMED_UNIT ( * ) SI_UNIT ( .MILLI., .METRE. ) );
#99658=SURFACE_STYLE_FILL_AREA ( #133051 ) ;
#101405=DIRECTION ( 'NONE',  ( 0.000000000000000000, 1.000000000000000000, 0.000000000000000000 ) ) ;
#102165=( GEOMETRIC_REPRESENTATION_CONTEXT ( 3 ) GLOBAL_UNCERTAINTY_ASSIGNED_CONTEXT ( ( #4207 ) ) GLOBAL_UNIT_ASSIGNED_CONTEXT ( ( #53487, #139075, #108531 ) ) REPRESENTATION_CONTEXT ( 'NONE', 'WORKASPACE' ) );
#102718=DIRECTION ( 'NONE',  ( 0.000000000000000000, 0.000000000000000000, 1.000000000000000000 ) ) ;
#102843=( NAMED_UNIT ( * ) PLANE_ANGLE_UNIT ( ) SI_UNIT ( $, .RADIAN. ) );
#104174=( NAMED_UNIT ( * ) SI_UNIT ( $, .STERADIAN. ) SOLID_ANGLE_UNIT ( ) );
#104221=FILL_AREA_STYLE ('',( #137613 ) ) ;
#104468=( NAMED_UNIT ( * ) SI_UNIT ( $, .STERADIAN. ) SOLID_ANGLE_UNIT ( ) );
#105608=PRESENTATION_STYLE_ASSIGNMENT (( #41092 ) ) ;
#106073=FILL_AREA_STYLE ('',( #61921 ) ) ;
#107309=ADVANCED_FACE ( 'NONE', ( #69510 ), #113700, .T. ) ;
#108309=ORIENTED_EDGE ( 'NONE', *, *, #75552, .T. ) ;
#108461=CARTESIAN_POINT ( 'NONE',  ( 4.898587196589412829E-16, 60.00000000000000000, 4.000000000000000000 ) ) ;
#108531=( NAMED_UNIT ( * ) SI_UNIT ( $, .STERADIAN. ) SOLID_ANGLE_UNIT ( ) );
#110119=CARTESIAN_POINT ( 'NONE',  ( 0.000000000000000000, 60.00000000000000000, 0.000000000000000000 ) ) ;
#110867=( GEOMETRIC_REPRESENTATION_CONTEXT ( 3 ) GLOBAL_UNCERTAINTY_ASSIGNED_CONTEXT ( ( #143330 ) ) GLOBAL_UNIT_ASSIGNED_CONTEXT ( ( #116059, #15293, #104468 ) ) REPRESENTATION_CONTEXT ( 'NONE', 'WORKASPACE' ) );
#111821=STYLED_ITEM ( 'NONE', ( #105608 ), #96673 ) ;
#112686=FACE_OUTER_BOUND ( 'NONE', #31111, .T. ) ;
#113700=CYLINDRICAL_SURFACE ( 'NONE', #68331, 4.000000000000000000 ) ;
#114060=EDGE_CURVE ( 'NONE', #115520, #76434, #131697, .T. ) ;
#114185=( GEOMETRIC_REPRESENTATION_CONTEXT ( 3 ) GLOBAL_UNCERTAINTY_ASSIGNED_CONTEXT ( ( #46024 ) ) GLOBAL_UNIT_ASSIGNED_CONTEXT ( ( #138273, #51274, #104174 ) ) REPRESENTATION_CONTEXT ( 'NONE', 'WORKASPACE' ) );
#115144=ORIENTED_EDGE ( 'NONE', *, *, #114060, .T. ) ;
#115309=FILL_AREA_STYLE_COLOUR ( '', #18245 ) ;
#115520=VERTEX_POINT ( 'NONE', #119914 ) ;
#116059=( LENGTH_UNIT ( ) NAMED_UNIT ( * ) SI_UNIT ( .MILLI., .METRE. ) );
#116779=SURFACE_STYLE_USAGE ( .BOTH. , #83456 ) ;
#116978=PLANE ( 'NONE',  #77999 ) ;
#117978=FACE_OUTER_BOUND ( 'NONE', #18771, .T. ) ;
#118726=PRESENTATION_STYLE_ASSIGNMENT (( #139809 ) ) ;
#119810=CARTESIAN_POINT ( 'NONE',  ( 0.000000000000000000, -60.00000000000000000, 0.000000000000000000 ) ) ;
#119914=CARTESIAN_POINT ( 'NONE',  ( 4.898587196589412829E-16, 60.00000000000000000, 4.000000000000000000 ) ) ;
#121561=( GEOMETRIC_REPRESENTATION_CONTEXT ( 3 ) GLOBAL_UNCERTAINTY_ASSIGNED_CONTEXT ( ( #67822 ) ) GLOBAL_UNIT_ASSIGNED_CONTEXT ( ( #14391, #102843, #70252 ) ) REPRESENTATION_CONTEXT ( 'NONE', 'WORKASPACE' ) );
#123180=DIRECTION ( 'NONE',  ( 0.000000000000000000, 0.000000000000000000, 1.000000000000000000 ) ) ;
#124580=PRESENTATION_STYLE_ASSIGNMENT (( #48446 ) ) ;
#126657=FILL_AREA_STYLE ('',( #93335 ) ) ;
#127137=MECHANICAL_DESIGN_GEOMETRIC_PRESENTATION_REPRESENTATION('',(#99284),#110867);
#127824=VECTOR ( 'NONE', #73030, 1000.000000000000000 ) ;
#127880=AXIS2_PLACEMENT_3D ( 'NONE', #8925, #141658, #53195 ) ;
#128082=( GEOMETRIC_REPRESENTATION_CONTEXT ( 3 ) GLOBAL_UNCERTAINTY_ASSIGNED_CONTEXT ( ( #74825 ) ) GLOBAL_UNIT_ASSIGNED_CONTEXT ( ( #73720, #71595, #83179 ) ) REPRESENTATION_CONTEXT ( 'NONE', 'WORKASPACE' ) );
#129076=UNCERTAINTY_MEASURE_WITH_UNIT (LENGTH_MEASURE( 1.000000000000000082E-05 ), #99489, 'distance_accuracy_value', 'NONE');
#130344=SURFACE_STYLE_FILL_AREA ( #94809 ) ;
#131697=LINE ( 'NONE', #108461, #50772 ) ;
#133051=FILL_AREA_STYLE ('',( #90964 ) ) ;
#134373=CIRCLE ( 'NONE', #25470, 4.000000000000000000 ) ;
#135364=CARTESIAN_POINT ( 'NONE',  ( 0.000000000000000000, -60.00000000000000000, 0.000000000000000000 ) ) ;
#136913=COLOUR_RGB ( '', 0.31764706, 0.68627451, 0.89019608) ;
#137613=FILL_AREA_STYLE_COLOUR ( '', #98405 ) ;
#137997=CARTESIAN_POINT ( 'NONE',  ( 0.000000000000000000, -60.00000000000000000, -4.000000000000000000 ) ) ;
#138273=( LENGTH_UNIT ( ) NAMED_UNIT ( * ) SI_UNIT ( .MILLI., .METRE. ) );
#138825=SHAPE_DEFINITION_REPRESENTATION ( #34012, #39429 ) ;
#139075=( NAMED_UNIT ( * ) PLANE_ANGLE_UNIT ( ) SI_UNIT ( $, .RADIAN. ) );
#139143=MANIFOLD_SOLID_BREP ( 'Boss-Extrude1', #71883 ) ;
#139728=SURFACE_SIDE_STYLE ('',( #140406 ) ) ;
#139809=SURFACE_STYLE_USAGE ( .BOTH. , #17956 ) ;
#140406=SURFACE_STYLE_FILL_AREA ( #126657 ) ;
#141297=CIRCLE ( 'NONE', #32558, 4.000000000000000000 ) ;
#141658=DIRECTION ( 'NONE',  ( 0.000000000000000000, 0.000000000000000000, 1.000000000000000000 ) ) ;
#143177=SURFACE_STYLE_USAGE ( .BOTH. , #79406 ) ;
#143330=UNCERTAINTY_MEASURE_WITH_UNIT (LENGTH_MEASURE( 1.000000000000000082E-05 ), #116059, 'distance_accuracy_value', 'NONE');
ENDSEC;
END-ISO-10303-21;
